ISO-10303-21;
HEADER;
/* Generated by software containing ST-Developer
 * from STEP Tools, Inc. (www.steptools.com) 
 */

FILE_DESCRIPTION(
/* description */ ('STEP AP214'),
/* implementation_level */ '2;1');

FILE_NAME(
/* name */ 'Ball Screw Support Plate.step',
/* time_stamp */ '2026-11-15T14:49:54-08:00',
/* author */ (''),
/* organization */ (''),
/* preprocessor_version */ 'ST-DEVELOPER v20.2',
/* originating_system */ 'Autodesk Translation Framework v15.17.0.0',
/* authorisation */ '');

FILE_SCHEMA (('AUTOMOTIVE_DESIGN { 1 0 10303 214 3 1 1 }'));
ENDSEC;

DATA;
#10=MECHANICAL_DESIGN_GEOMETRIC_PRESENTATION_REPRESENTATION('',(#1102),#66721);
#1040=SHAPE_REPRESENTATION_RELATIONSHIP('SRR','None',#66897,#1071);
#1071=ADVANCED_BREP_SHAPE_REPRESENTATION('',(#1137),#66688);
#1102=STYLED_ITEM('',(#67095),#1137);
#1137=MANIFOLD_SOLID_BREP('Body1',#25668);
#1223=FACE_BOUND('',#3847,.T.);
#1224=FACE_BOUND('',#3848,.T.);
#1225=FACE_BOUND('',#3849,.T.);
#1226=FACE_BOUND('',#3850,.T.);
#1227=FACE_BOUND('',#3851,.T.);
#1228=FACE_BOUND('',#3852,.T.);
#1229=FACE_BOUND('',#3854,.T.);
#1230=FACE_BOUND('',#3855,.T.);
#1231=FACE_BOUND('',#3856,.T.);
#1232=FACE_BOUND('',#3857,.T.);
#1233=FACE_BOUND('',#3858,.T.);
#1234=FACE_BOUND('',#3859,.T.);
#1539=PLANE('',#26195);
#1540=PLANE('',#26196);
#1541=PLANE('',#26197);
#1542=PLANE('',#26198);
#1543=PLANE('',#26199);
#1544=PLANE('',#26200);
#2339=FACE_OUTER_BOUND('',#3836,.T.);
#2340=FACE_OUTER_BOUND('',#3837,.T.);
#2341=FACE_OUTER_BOUND('',#3838,.T.);
#2342=FACE_OUTER_BOUND('',#3839,.T.);
#2343=FACE_OUTER_BOUND('',#3840,.T.);
#2344=FACE_OUTER_BOUND('',#3841,.T.);
#2345=FACE_OUTER_BOUND('',#3842,.T.);
#2346=FACE_OUTER_BOUND('',#3843,.T.);
#2347=FACE_OUTER_BOUND('',#3844,.T.);
#2348=FACE_OUTER_BOUND('',#3845,.T.);
#2349=FACE_OUTER_BOUND('',#3846,.T.);
#2350=FACE_OUTER_BOUND('',#3853,.T.);
#3836=EDGE_LOOP('',(#16948,#16949,#16950,#16951));
#3837=EDGE_LOOP('',(#16952,#16953,#16954,#16955));
#3838=EDGE_LOOP('',(#16956,#16957,#16958,#16959));
#3839=EDGE_LOOP('',(#16960,#16961,#16962,#16963));
#3840=EDGE_LOOP('',(#16964,#16965,#16966,#16967));
#3841=EDGE_LOOP('',(#16968,#16969,#16970,#16971));
#3842=EDGE_LOOP('',(#16972,#16973,#16974,#16975));
#3843=EDGE_LOOP('',(#16976,#16977,#16978,#16979));
#3844=EDGE_LOOP('',(#16980,#16981,#16982,#16983));
#3845=EDGE_LOOP('',(#16984,#16985,#16986,#16987));
#3846=EDGE_LOOP('',(#16988,#16989,#16990,#16991));
#3847=EDGE_LOOP('',(#16992));
#3848=EDGE_LOOP('',(#16993));
#3849=EDGE_LOOP('',(#16994));
#3850=EDGE_LOOP('',(#16995));
#3851=EDGE_LOOP('',(#16996));
#3852=EDGE_LOOP('',(#16997));
#3853=EDGE_LOOP('',(#16998,#16999,#17000,#17001));
#3854=EDGE_LOOP('',(#17002));
#3855=EDGE_LOOP('',(#17003));
#3856=EDGE_LOOP('',(#17004));
#3857=EDGE_LOOP('',(#17005));
#3858=EDGE_LOOP('',(#17006));
#3859=EDGE_LOOP('',(#17007));
#5602=LINE('',#36552,#7591);
#5603=LINE('',#36558,#7592);
#5604=LINE('',#36564,#7593);
#5605=LINE('',#36570,#7594);
#5606=LINE('',#36576,#7595);
#5607=LINE('',#36582,#7596);
#5608=LINE('',#36587,#7597);
#5609=LINE('',#36589,#7598);
#5610=LINE('',#36591,#7599);
#5611=LINE('',#36592,#7600);
#5612=LINE('',#36595,#7601);
#5613=LINE('',#36597,#7602);
#5614=LINE('',#36598,#7603);
#5615=LINE('',#36601,#7604);
#5616=LINE('',#36603,#7605);
#5617=LINE('',#36604,#7606);
#5618=LINE('',#36606,#7607);
#5619=LINE('',#36607,#7608);
#7591=VECTOR('',#29151,2.99999999999999);
#7592=VECTOR('',#29158,2.99999999999999);
#7593=VECTOR('',#29165,3.3);
#7594=VECTOR('',#29172,3.3);
#7595=VECTOR('',#29179,3.3);
#7596=VECTOR('',#29186,3.3);
#7597=VECTOR('',#29191,1000.);
#7598=VECTOR('',#29192,1000.);
#7599=VECTOR('',#29193,1000.);
#7600=VECTOR('',#29194,1000.);
#7601=VECTOR('',#29197,1000.);
#7602=VECTOR('',#29198,1000.);
#7603=VECTOR('',#29199,1000.);
#7604=VECTOR('',#29202,1000.);
#7605=VECTOR('',#29203,1000.);
#7606=VECTOR('',#29204,1000.);
#7607=VECTOR('',#29207,1000.);
#7608=VECTOR('',#29208,1000.);
#9519=CIRCLE('',#26178,2.99999999999999);
#9520=CIRCLE('',#26179,2.99999999999999);
#9521=CIRCLE('',#26181,2.99999999999999);
#9522=CIRCLE('',#26182,2.99999999999999);
#9523=CIRCLE('',#26184,3.3);
#9524=CIRCLE('',#26185,3.3);
#9525=CIRCLE('',#26187,3.3);
#9526=CIRCLE('',#26188,3.3);
#9527=CIRCLE('',#26190,3.3);
#9528=CIRCLE('',#26191,3.3);
#9529=CIRCLE('',#26193,3.3);
#9530=CIRCLE('',#26194,3.3);
#10756=VERTEX_POINT('',#36549);
#10757=VERTEX_POINT('',#36551);
#10758=VERTEX_POINT('',#36555);
#10759=VERTEX_POINT('',#36557);
#10760=VERTEX_POINT('',#36561);
#10761=VERTEX_POINT('',#36563);
#10762=VERTEX_POINT('',#36567);
#10763=VERTEX_POINT('',#36569);
#10764=VERTEX_POINT('',#36573);
#10765=VERTEX_POINT('',#36575);
#10766=VERTEX_POINT('',#36579);
#10767=VERTEX_POINT('',#36581);
#10768=VERTEX_POINT('',#36585);
#10769=VERTEX_POINT('',#36586);
#10770=VERTEX_POINT('',#36588);
#10771=VERTEX_POINT('',#36590);
#10772=VERTEX_POINT('',#36594);
#10773=VERTEX_POINT('',#36596);
#10774=VERTEX_POINT('',#36600);
#10775=VERTEX_POINT('',#36602);
#13167=EDGE_CURVE('',#10756,#10756,#9519,.T.);
#13168=EDGE_CURVE('',#10756,#10757,#5602,.T.);
#13169=EDGE_CURVE('',#10757,#10757,#9520,.T.);
#13170=EDGE_CURVE('',#10758,#10758,#9521,.T.);
#13171=EDGE_CURVE('',#10758,#10759,#5603,.T.);
#13172=EDGE_CURVE('',#10759,#10759,#9522,.T.);
#13173=EDGE_CURVE('',#10760,#10760,#9523,.T.);
#13174=EDGE_CURVE('',#10760,#10761,#5604,.T.);
#13175=EDGE_CURVE('',#10761,#10761,#9524,.T.);
#13176=EDGE_CURVE('',#10762,#10762,#9525,.T.);
#13177=EDGE_CURVE('',#10762,#10763,#5605,.T.);
#13178=EDGE_CURVE('',#10763,#10763,#9526,.T.);
#13179=EDGE_CURVE('',#10764,#10764,#9527,.T.);
#13180=EDGE_CURVE('',#10764,#10765,#5606,.T.);
#13181=EDGE_CURVE('',#10765,#10765,#9528,.T.);
#13182=EDGE_CURVE('',#10766,#10766,#9529,.T.);
#13183=EDGE_CURVE('',#10766,#10767,#5607,.T.);
#13184=EDGE_CURVE('',#10767,#10767,#9530,.T.);
#13185=EDGE_CURVE('',#10768,#10769,#5608,.T.);
#13186=EDGE_CURVE('',#10770,#10769,#5609,.T.);
#13187=EDGE_CURVE('',#10771,#10770,#5610,.T.);
#13188=EDGE_CURVE('',#10771,#10768,#5611,.T.);
#13189=EDGE_CURVE('',#10769,#10772,#5612,.T.);
#13190=EDGE_CURVE('',#10773,#10772,#5613,.T.);
#13191=EDGE_CURVE('',#10770,#10773,#5614,.T.);
#13192=EDGE_CURVE('',#10772,#10774,#5615,.T.);
#13193=EDGE_CURVE('',#10775,#10774,#5616,.T.);
#13194=EDGE_CURVE('',#10773,#10775,#5617,.T.);
#13195=EDGE_CURVE('',#10774,#10768,#5618,.T.);
#13196=EDGE_CURVE('',#10775,#10771,#5619,.T.);
#16948=ORIENTED_EDGE('',*,*,#13167,.F.);
#16949=ORIENTED_EDGE('',*,*,#13168,.T.);
#16950=ORIENTED_EDGE('',*,*,#13169,.T.);
#16951=ORIENTED_EDGE('',*,*,#13168,.F.);
#16952=ORIENTED_EDGE('',*,*,#13170,.F.);
#16953=ORIENTED_EDGE('',*,*,#13171,.T.);
#16954=ORIENTED_EDGE('',*,*,#13172,.T.);
#16955=ORIENTED_EDGE('',*,*,#13171,.F.);
#16956=ORIENTED_EDGE('',*,*,#13173,.F.);
#16957=ORIENTED_EDGE('',*,*,#13174,.T.);
#16958=ORIENTED_EDGE('',*,*,#13175,.T.);
#16959=ORIENTED_EDGE('',*,*,#13174,.F.);
#16960=ORIENTED_EDGE('',*,*,#13176,.F.);
#16961=ORIENTED_EDGE('',*,*,#13177,.T.);
#16962=ORIENTED_EDGE('',*,*,#13178,.T.);
#16963=ORIENTED_EDGE('',*,*,#13177,.F.);
#16964=ORIENTED_EDGE('',*,*,#13179,.F.);
#16965=ORIENTED_EDGE('',*,*,#13180,.T.);
#16966=ORIENTED_EDGE('',*,*,#13181,.T.);
#16967=ORIENTED_EDGE('',*,*,#13180,.F.);
#16968=ORIENTED_EDGE('',*,*,#13182,.F.);
#16969=ORIENTED_EDGE('',*,*,#13183,.T.);
#16970=ORIENTED_EDGE('',*,*,#13184,.T.);
#16971=ORIENTED_EDGE('',*,*,#13183,.F.);
#16972=ORIENTED_EDGE('',*,*,#13185,.T.);
#16973=ORIENTED_EDGE('',*,*,#13186,.F.);
#16974=ORIENTED_EDGE('',*,*,#13187,.F.);
#16975=ORIENTED_EDGE('',*,*,#13188,.T.);
#16976=ORIENTED_EDGE('',*,*,#13189,.T.);
#16977=ORIENTED_EDGE('',*,*,#13190,.F.);
#16978=ORIENTED_EDGE('',*,*,#13191,.F.);
#16979=ORIENTED_EDGE('',*,*,#13186,.T.);
#16980=ORIENTED_EDGE('',*,*,#13192,.T.);
#16981=ORIENTED_EDGE('',*,*,#13193,.F.);
#16982=ORIENTED_EDGE('',*,*,#13194,.F.);
#16983=ORIENTED_EDGE('',*,*,#13190,.T.);
#16984=ORIENTED_EDGE('',*,*,#13195,.T.);
#16985=ORIENTED_EDGE('',*,*,#13188,.F.);
#16986=ORIENTED_EDGE('',*,*,#13196,.F.);
#16987=ORIENTED_EDGE('',*,*,#13193,.T.);
#16988=ORIENTED_EDGE('',*,*,#13187,.T.);
#16989=ORIENTED_EDGE('',*,*,#13191,.T.);
#16990=ORIENTED_EDGE('',*,*,#13194,.T.);
#16991=ORIENTED_EDGE('',*,*,#13196,.T.);
#16992=ORIENTED_EDGE('',*,*,#13169,.F.);
#16993=ORIENTED_EDGE('',*,*,#13172,.F.);
#16994=ORIENTED_EDGE('',*,*,#13175,.F.);
#16995=ORIENTED_EDGE('',*,*,#13178,.F.);
#16996=ORIENTED_EDGE('',*,*,#13181,.F.);
#16997=ORIENTED_EDGE('',*,*,#13184,.F.);
#16998=ORIENTED_EDGE('',*,*,#13185,.F.);
#16999=ORIENTED_EDGE('',*,*,#13195,.F.);
#17000=ORIENTED_EDGE('',*,*,#13192,.F.);
#17001=ORIENTED_EDGE('',*,*,#13189,.F.);
#17002=ORIENTED_EDGE('',*,*,#13167,.T.);
#17003=ORIENTED_EDGE('',*,*,#13170,.T.);
#17004=ORIENTED_EDGE('',*,*,#13173,.T.);
#17005=ORIENTED_EDGE('',*,*,#13176,.T.);
#17006=ORIENTED_EDGE('',*,*,#13179,.T.);
#17007=ORIENTED_EDGE('',*,*,#13182,.T.);
#23831=CYLINDRICAL_SURFACE('',#26177,2.99999999999999);
#23832=CYLINDRICAL_SURFACE('',#26180,2.99999999999999);
#23833=CYLINDRICAL_SURFACE('',#26183,3.3);
#23834=CYLINDRICAL_SURFACE('',#26186,3.3);
#23835=CYLINDRICAL_SURFACE('',#26189,3.3);
#23836=CYLINDRICAL_SURFACE('',#26192,3.3);
#24292=ADVANCED_FACE('',(#2339),#23831,.F.);
#24293=ADVANCED_FACE('',(#2340),#23832,.F.);
#24294=ADVANCED_FACE('',(#2341),#23833,.F.);
#24295=ADVANCED_FACE('',(#2342),#23834,.F.);
#24296=ADVANCED_FACE('',(#2343),#23835,.F.);
#24297=ADVANCED_FACE('',(#2344),#23836,.F.);
#24298=ADVANCED_FACE('',(#2345),#1539,.F.);
#24299=ADVANCED_FACE('',(#2346),#1540,.F.);
#24300=ADVANCED_FACE('',(#2347),#1541,.F.);
#24301=ADVANCED_FACE('',(#2348),#1542,.F.);
#24302=ADVANCED_FACE('',(#2349,#1223,#1224,#1225,#1226,#1227,#1228),#1543,
 .T.);
#24303=ADVANCED_FACE('',(#2350,#1229,#1230,#1231,#1232,#1233,#1234),#1544,
 .F.);
#25668=CLOSED_SHELL('',(#24292,#24293,#24294,#24295,#24296,#24297,#24298,
#24299,#24300,#24301,#24302,#24303));
#26176=AXIS2_PLACEMENT_3D('',#36547,#29145,#29146);
#26177=AXIS2_PLACEMENT_3D('',#36548,#29147,#29148);
#26178=AXIS2_PLACEMENT_3D('',#36550,#29149,#29150);
#26179=AXIS2_PLACEMENT_3D('',#36553,#29152,#29153);
#26180=AXIS2_PLACEMENT_3D('',#36554,#29154,#29155);
#26181=AXIS2_PLACEMENT_3D('',#36556,#29156,#29157);
#26182=AXIS2_PLACEMENT_3D('',#36559,#29159,#29160);
#26183=AXIS2_PLACEMENT_3D('',#36560,#29161,#29162);
#26184=AXIS2_PLACEMENT_3D('',#36562,#29163,#29164);
#26185=AXIS2_PLACEMENT_3D('',#36565,#29166,#29167);
#26186=AXIS2_PLACEMENT_3D('',#36566,#29168,#29169);
#26187=AXIS2_PLACEMENT_3D('',#36568,#29170,#29171);
#26188=AXIS2_PLACEMENT_3D('',#36571,#29173,#29174);
#26189=AXIS2_PLACEMENT_3D('',#36572,#29175,#29176);
#26190=AXIS2_PLACEMENT_3D('',#36574,#29177,#29178);
#26191=AXIS2_PLACEMENT_3D('',#36577,#29180,#29181);
#26192=AXIS2_PLACEMENT_3D('',#36578,#29182,#29183);
#26193=AXIS2_PLACEMENT_3D('',#36580,#29184,#29185);
#26194=AXIS2_PLACEMENT_3D('',#36583,#29187,#29188);
#26195=AXIS2_PLACEMENT_3D('',#36584,#29189,#29190);
#26196=AXIS2_PLACEMENT_3D('',#36593,#29195,#29196);
#26197=AXIS2_PLACEMENT_3D('',#36599,#29200,#29201);
#26198=AXIS2_PLACEMENT_3D('',#36605,#29205,#29206);
#26199=AXIS2_PLACEMENT_3D('',#36608,#29209,#29210);
#26200=AXIS2_PLACEMENT_3D('',#36609,#29211,#29212);
#29145=DIRECTION('axis',(0.,0.,1.));
#29146=DIRECTION('refdir',(1.,0.,0.));
#29147=DIRECTION('center_axis',(0.,0.,1.));
#29148=DIRECTION('ref_axis',(1.,0.,0.));
#29149=DIRECTION('center_axis',(0.,0.,1.));
#29150=DIRECTION('ref_axis',(1.,0.,0.));
#29151=DIRECTION('',(0.,0.,1.));
#29152=DIRECTION('center_axis',(0.,0.,1.));
#29153=DIRECTION('ref_axis',(1.,0.,0.));
#29154=DIRECTION('center_axis',(0.,0.,1.));
#29155=DIRECTION('ref_axis',(1.,0.,0.));
#29156=DIRECTION('center_axis',(0.,0.,1.));
#29157=DIRECTION('ref_axis',(1.,0.,0.));
#29158=DIRECTION('',(0.,0.,1.));
#29159=DIRECTION('center_axis',(0.,0.,1.));
#29160=DIRECTION('ref_axis',(1.,0.,0.));
#29161=DIRECTION('center_axis',(0.,0.,1.));
#29162=DIRECTION('ref_axis',(1.,0.,0.));
#29163=DIRECTION('center_axis',(0.,0.,1.));
#29164=DIRECTION('ref_axis',(1.,0.,0.));
#29165=DIRECTION('',(0.,0.,1.));
#29166=DIRECTION('center_axis',(0.,0.,1.));
#29167=DIRECTION('ref_axis',(1.,0.,0.));
#29168=DIRECTION('center_axis',(0.,0.,1.));
#29169=DIRECTION('ref_axis',(1.,0.,0.));
#29170=DIRECTION('center_axis',(0.,0.,1.));
#29171=DIRECTION('ref_axis',(1.,0.,0.));
#29172=DIRECTION('',(0.,0.,1.));
#29173=DIRECTION('center_axis',(0.,0.,1.));
#29174=DIRECTION('ref_axis',(1.,0.,0.));
#29175=DIRECTION('center_axis',(0.,0.,1.));
#29176=DIRECTION('ref_axis',(1.,0.,0.));
#29177=DIRECTION('center_axis',(0.,0.,1.));
#29178=DIRECTION('ref_axis',(1.,0.,0.));
#29179=DIRECTION('',(0.,0.,1.));
#29180=DIRECTION('center_axis',(0.,0.,1.));
#29181=DIRECTION('ref_axis',(1.,0.,0.));
#29182=DIRECTION('center_axis',(0.,0.,1.));
#29183=DIRECTION('ref_axis',(1.,0.,0.));
#29184=DIRECTION('center_axis',(0.,0.,1.));
#29185=DIRECTION('ref_axis',(1.,0.,0.));
#29186=DIRECTION('',(0.,0.,1.));
#29187=DIRECTION('center_axis',(0.,0.,1.));
#29188=DIRECTION('ref_axis',(1.,0.,0.));
#29189=DIRECTION('center_axis',(-1.,-1.46081976924363E-16,0.));
#29190=DIRECTION('ref_axis',(1.46081976924363E-16,-1.,0.));
#29191=DIRECTION('',(-1.46081976924363E-16,1.,0.));
#29192=DIRECTION('',(0.,0.,-1.));
#29193=DIRECTION('',(-1.46081976924363E-16,1.,0.));
#29194=DIRECTION('',(0.,0.,-1.));
#29195=DIRECTION('center_axis',(0.,-1.,0.));
#29196=DIRECTION('ref_axis',(0.,0.,-1.));
#29197=DIRECTION('',(-1.,0.,0.));
#29198=DIRECTION('',(0.,0.,-1.));
#29199=DIRECTION('',(-1.,0.,0.));
#29200=DIRECTION('center_axis',(1.,1.46081976924363E-16,0.));
#29201=DIRECTION('ref_axis',(-1.46081976924363E-16,1.,0.));
#29202=DIRECTION('',(1.46081976924363E-16,-1.,0.));
#29203=DIRECTION('',(0.,0.,-1.));
#29204=DIRECTION('',(1.46081976924363E-16,-1.,0.));
#29205=DIRECTION('center_axis',(0.,1.,0.));
#29206=DIRECTION('ref_axis',(0.,0.,1.));
#29207=DIRECTION('',(1.,0.,0.));
#29208=DIRECTION('',(1.,0.,0.));
#29209=DIRECTION('center_axis',(0.,0.,1.));
#29210=DIRECTION('ref_axis',(1.,0.,0.));
#29211=DIRECTION('center_axis',(0.,0.,1.));
#29212=DIRECTION('ref_axis',(1.,0.,0.));
#36547=CARTESIAN_POINT('',(0.,0.,0.));
#36548=CARTESIAN_POINT('Origin',(-20.,33.,5.));
#36549=CARTESIAN_POINT('',(-23.,33.,-5.));
#36550=CARTESIAN_POINT('Origin',(-20.,33.,-5.));
#36551=CARTESIAN_POINT('',(-23.,33.,5.));
#36552=CARTESIAN_POINT('',(-23.,33.,5.));
#36553=CARTESIAN_POINT('Origin',(-20.,33.,5.));
#36554=CARTESIAN_POINT('Origin',(20.,-33.,5.));
#36555=CARTESIAN_POINT('',(17.,-33.,-5.));
#36556=CARTESIAN_POINT('Origin',(20.,-33.,-5.));
#36557=CARTESIAN_POINT('',(17.,-33.,5.));
#36558=CARTESIAN_POINT('',(17.,-33.,5.));
#36559=CARTESIAN_POINT('Origin',(20.,-33.,5.));
#36560=CARTESIAN_POINT('Origin',(40.,33.,5.));
#36561=CARTESIAN_POINT('',(36.7,33.,-5.));
#36562=CARTESIAN_POINT('Origin',(40.,33.,-5.));
#36563=CARTESIAN_POINT('',(36.7,33.,5.));
#36564=CARTESIAN_POINT('',(36.7,33.,5.));
#36565=CARTESIAN_POINT('Origin',(40.,33.,5.));
#36566=CARTESIAN_POINT('Origin',(-40.,33.,5.));
#36567=CARTESIAN_POINT('',(-43.3,33.,-5.));
#36568=CARTESIAN_POINT('Origin',(-40.,33.,-5.));
#36569=CARTESIAN_POINT('',(-43.3,33.,5.));
#36570=CARTESIAN_POINT('',(-43.3,33.,5.));
#36571=CARTESIAN_POINT('Origin',(-40.,33.,5.));
#36572=CARTESIAN_POINT('Origin',(-40.,-33.,5.));
#36573=CARTESIAN_POINT('',(-43.3,-33.,-5.));
#36574=CARTESIAN_POINT('Origin',(-40.,-33.,-5.));
#36575=CARTESIAN_POINT('',(-43.3,-33.,5.));
#36576=CARTESIAN_POINT('',(-43.3,-33.,5.));
#36577=CARTESIAN_POINT('Origin',(-40.,-33.,5.));
#36578=CARTESIAN_POINT('Origin',(40.,-33.,5.));
#36579=CARTESIAN_POINT('',(36.7,-33.,-5.));
#36580=CARTESIAN_POINT('Origin',(40.,-33.,-5.));
#36581=CARTESIAN_POINT('',(36.7,-33.,5.));
#36582=CARTESIAN_POINT('',(36.7,-33.,5.));
#36583=CARTESIAN_POINT('Origin',(40.,-33.,5.));
#36584=CARTESIAN_POINT('Origin',(55.,47.5,5.));
#36585=CARTESIAN_POINT('',(55.,-47.5,-5.));
#36586=CARTESIAN_POINT('',(55.,47.5,-5.));
#36587=CARTESIAN_POINT('',(55.,47.5,-5.));
#36588=CARTESIAN_POINT('',(55.,47.5,5.));
#36589=CARTESIAN_POINT('',(55.,47.5,5.));
#36590=CARTESIAN_POINT('',(55.,-47.5,5.));
#36591=CARTESIAN_POINT('',(55.,47.5,5.));
#36592=CARTESIAN_POINT('',(55.,-47.5,5.));
#36593=CARTESIAN_POINT('Origin',(-55.,47.5,5.));
#36594=CARTESIAN_POINT('',(-55.,47.5,-5.));
#36595=CARTESIAN_POINT('',(-55.,47.5,-5.));
#36596=CARTESIAN_POINT('',(-55.,47.5,5.));
#36597=CARTESIAN_POINT('',(-55.,47.5,5.));
#36598=CARTESIAN_POINT('',(-55.,47.5,5.));
#36599=CARTESIAN_POINT('Origin',(-55.,47.5,5.));
#36600=CARTESIAN_POINT('',(-55.,-47.5,-5.));
#36601=CARTESIAN_POINT('',(-55.,47.5,-5.));
#36602=CARTESIAN_POINT('',(-55.,-47.5,5.));
#36603=CARTESIAN_POINT('',(-55.,-47.5,5.));
#36604=CARTESIAN_POINT('',(-55.,47.5,5.));
#36605=CARTESIAN_POINT('Origin',(-55.,-47.5,5.));
#36606=CARTESIAN_POINT('',(-55.,-47.5,-5.));
#36607=CARTESIAN_POINT('',(-55.,-47.5,5.));
#36608=CARTESIAN_POINT('Origin',(0.,0.,5.));
#36609=CARTESIAN_POINT('Origin',(0.,0.,-5.));
#66647=UNCERTAINTY_MEASURE_WITH_UNIT(LENGTH_MEASURE(0.01),#66722,
'DISTANCE_ACCURACY_VALUE',
'Maximum model space distance between geometric entities at asserted c
onnectivities');
#66680=UNCERTAINTY_MEASURE_WITH_UNIT(LENGTH_MEASURE(0.01),#66722,
'DISTANCE_ACCURACY_VALUE',
'Maximum model space distance between geometric entities at asserted c
onnectivities');
#66688=(
GEOMETRIC_REPRESENTATION_CONTEXT(3)
GLOBAL_UNCERTAINTY_ASSIGNED_CONTEXT((#66647))
GLOBAL_UNIT_ASSIGNED_CONTEXT((#66722,#66724,#66725))
REPRESENTATION_CONTEXT('','3D')
);
#66721=(
GEOMETRIC_REPRESENTATION_CONTEXT(3)
GLOBAL_UNCERTAINTY_ASSIGNED_CONTEXT((#66680))
GLOBAL_UNIT_ASSIGNED_CONTEXT((#66722,#66724,#66725))
REPRESENTATION_CONTEXT('','3D')
);
#66722=(
LENGTH_UNIT()
NAMED_UNIT(*)
SI_UNIT(.MILLI.,.METRE.)
);
#66724=(
NAMED_UNIT(*)
PLANE_ANGLE_UNIT()
SI_UNIT($,.RADIAN.)
);
#66725=(
NAMED_UNIT(*)
SI_UNIT($,.STERADIAN.)
SOLID_ANGLE_UNIT()
);
#66733=SHAPE_DEFINITION_REPRESENTATION(#66773,#66897);
#66773=PRODUCT_DEFINITION_SHAPE('',$,#66938);
#66897=SHAPE_REPRESENTATION('',(#26176),#66688);
#66930=PRODUCT_DEFINITION_CONTEXT('part definition',#67052,'design');
#66938=PRODUCT_DEFINITION('Ball Screw Support Plate',
'Ball Screw Support Plate',#66978,#66930);
#66978=PRODUCT_DEFINITION_FORMATION('',$,#67061);
#67052=APPLICATION_CONTEXT(
'Core Data for Automotive Mechanical Design Process');
#67053=PRODUCT_CONTEXT('part definition',#67052,'mechanical');
#67061=PRODUCT('Ball Screw Support Plate','Ball Screw Support Plate',$,
(#67053));
#67095=PRESENTATION_STYLE_ASSIGNMENT((#67097));
#67097=SURFACE_STYLE_USAGE(.BOTH.,#67099);
#67099=SURFACE_SIDE_STYLE('',(#67101));
#67101=SURFACE_STYLE_FILL_AREA(#67103);
#67103=FILL_AREA_STYLE('Opaque(202,209,238)',(#67105));
#67105=FILL_AREA_STYLE_COLOUR('Opaque(202,209,238)',#67107);
#67107=COLOUR_RGB('Opaque(202,209,238)',0.792156862745098,0.819607843137255,
0.933333333333333);
ENDSEC;
END-ISO-10303-21;
